ISO-10303-21;
HEADER;
FILE_DESCRIPTION (('STEP AP214'),
    '1' );
FILE_NAME ('slotted cheese head screw_iso_ISO 1207 - M10 x 35 - 35N.step',
    '2026-10-24T00:09:50',
    ( '' ),
    ( '' ),
    'SwSTEP 2.0',
    'SolidWorks 2025',
    '' );
FILE_SCHEMA (( 'AUTOMOTIVE_DESIGN' ));
ENDSEC;

DATA;
#14=VECTOR ( 'NONE', #24941, 1000.000000000000000 ) ;
#154=ORIENTED_EDGE ( 'NONE', *, *, #16207, .F. ) ;
#379=ORIENTED_EDGE ( 'NONE', *, *, #16079, .F. ) ;
#388=CARTESIAN_POINT ( 'NONE',  ( 1.250275373174978277, -1.249999999999998890, -7.480737022738205511 ) ) ;
#427=CARTESIAN_POINT ( 'NONE',  ( 0.3999999999999999667, 0.000000000000000000, 0.000000000000000000 ) ) ;
#451=CIRCLE ( 'NONE', #6855, 5.000000000000000000 ) ;
#553=VERTEX_POINT ( 'NONE', #7053 ) ;
#669=DIRECTION ( 'NONE',  ( 0.000000000000000000, 0.000000000000000000, 1.000000000000000000 ) ) ;
#761=VERTEX_POINT ( 'NONE', #16391 ) ;
#779=ADVANCED_FACE ( 'NONE', ( #18261 ), #9781, .T. ) ;
#840=UNCERTAINTY_MEASURE_WITH_UNIT (LENGTH_MEASURE( 1.000000000000000082E-05 ), #2464, 'distance_accuracy_value', 'NONE');
#874=VECTOR ( 'NONE', #17839, 1000.000000000000000 ) ;
#1032=DIRECTION ( 'NONE',  ( -1.000000000000000000, 0.000000000000000000, -0.000000000000000000 ) ) ;
#1172=CARTESIAN_POINT ( 'NONE',  ( 40.99999999999999289, 0.000000000000000000, 0.000000000000000000 ) ) ;
#1193=ORIENTED_EDGE ( 'NONE', *, *, #23218, .T. ) ;
#1201=ORIENTED_EDGE ( 'NONE', *, *, #15008, .T. ) ;
#1312=DIRECTION ( 'NONE',  ( -0.000000000000000000, 0.000000000000000000, 1.000000000000000000 ) ) ;
#1317=CIRCLE ( 'NONE', #14176, 7.685040811306672381 ) ;
#1379=CARTESIAN_POINT ( 'NONE',  ( 0.2652980290584672218, 1.249999999999999778, -7.393354040734018362 ) ) ;
#1452=EDGE_CURVE ( 'NONE', #24464, #6433, #3888, .T. ) ;
#1506=TOROIDAL_SURFACE ( 'NONE', #27199, 7.108535549237485540, 0.4000000000000000222 ) ;
#1547=PRODUCT ( 'slotted cheese head screw_iso_ISO 1207 - M10 x 35 - 35N', 'slotted cheese head screw_iso_ISO 1207 - M10 x 35 - 35N', '', ( #10217 ) ) ;
#1600=VERTEX_POINT ( 'NONE', #14308 ) ;
#1625=DIRECTION ( 'NONE',  ( 1.000000000000000000, 0.000000000000000000, 0.000000000000000000 ) ) ;
#1632=ORIENTED_EDGE ( 'NONE', *, *, #5428, .T. ) ;
#1788=VERTEX_POINT ( 'NONE', #2478 ) ;
#1789=CARTESIAN_POINT ( 'NONE',  ( 0.3651377029009472142, 1.249999999999999556, -7.402212548643259282 ) ) ;
#1865=CIRCLE ( 'NONE', #25736, 7.685040811306672381 ) ;
#1901=ORIENTED_EDGE ( 'NONE', *, *, #16079, .T. ) ;
#1984=ORIENTED_EDGE ( 'NONE', *, *, #18001, .T. ) ;
#2061=CARTESIAN_POINT ( 'NONE',  ( 0.000000000000000000, 1.249999999999999556, 6.997769477110050929 ) ) ;
#2218=VERTEX_POINT ( 'NONE', #6877 ) ;
#2220=FACE_OUTER_BOUND ( 'NONE', #11224, .T. ) ;
#2251=PLANE ( 'NONE',  #12927 ) ;
#2320=DIRECTION ( 'NONE',  ( 0.000000000000000000, 0.000000000000000000, 1.000000000000000000 ) ) ;
#2435=ORIENTED_EDGE ( 'NONE', *, *, #8743, .F. ) ;
#2464=( LENGTH_UNIT ( ) NAMED_UNIT ( * ) SI_UNIT ( .MILLI., .METRE. ) );
#2469=VECTOR ( 'NONE', #25107, 1000.000000000000000 ) ;
#2478=CARTESIAN_POINT ( 'NONE',  ( 0.3651377029009472142, 1.249999999999999556, -7.402212548643259282 ) ) ;
#2665=CARTESIAN_POINT ( 'NONE',  ( 5.999999999999998224, 0.000000000000000000, 0.000000000000000000 ) ) ;
#2711=FACE_OUTER_BOUND ( 'NONE', #28224, .T. ) ;
#2853=DIRECTION ( 'NONE',  ( 0.000000000000000000, 0.000000000000000000, -1.000000000000000000 ) ) ;
#3050=AXIS2_PLACEMENT_3D ( 'NONE', #6788, #8671, #15569 ) ;
#3112=ORIENTED_EDGE ( 'NONE', *, *, #27376, .T. ) ;
#3171=ORIENTED_EDGE ( 'NONE', *, *, #23218, .F. ) ;
#3240=MECHANICAL_DESIGN_GEOMETRIC_PRESENTATION_REPRESENTATION('',(#4160),#14743);
#3245=ORIENTED_EDGE ( 'NONE', *, *, #6358, .T. ) ;
#3254=VERTEX_POINT ( 'NONE', #24721 ) ;
#3380=CARTESIAN_POINT ( 'NONE',  ( -1.445038208015836378E-15, -1.249999999999998890, -7.096885197977455206 ) ) ;
#3461=CARTESIAN_POINT ( 'NONE',  ( -6.124983682450844166E-17, 0.000000000000000000, 0.000000000000000000 ) ) ;
#3532=B_SPLINE_CURVE_WITH_KNOTS ( 'NONE', 3,
 ( #25769, #19167, #15156, #23482, #23909, #2061 ),
 .UNSPECIFIED., .F., .F.,
 ( 4, 2, 4 ),
 ( 0.001556600976750998223, 0.001854275657213667883, 0.002151950337676337543 ),
 .UNSPECIFIED. ) ;
#3601=ORIENTED_EDGE ( 'NONE', *, *, #25333, .T. ) ;
#3626=DIRECTION ( 'NONE',  ( -1.000000000000000000, 0.000000000000000000, -0.000000000000000000 ) ) ;
#3627=ORIENTED_EDGE ( 'NONE', *, *, #16737, .T. ) ;
#3645=VERTEX_POINT ( 'NONE', #15727 ) ;
#3664=CARTESIAN_POINT ( 'NONE',  ( 2.399999999999999911, 0.000000000000000000, 0.000000000000000000 ) ) ;
#3812=CARTESIAN_POINT ( 'NONE',  ( 2.399999999999999911, -1.250000000000000444, 7.582700855991164168 ) ) ;
#3837=AXIS2_PLACEMENT_3D ( 'NONE', #4626, #21883, #13414 ) ;
#3858=VERTEX_POINT ( 'NONE', #27051 ) ;
#3888=CIRCLE ( 'NONE', #18140, 5.000000000000000000 ) ;
#4067=PRODUCT_DEFINITION_SHAPE ( 'NONE', 'NONE',  #25635 ) ;
#4160=STYLED_ITEM('',(#28448),#18502);
#4232=CARTESIAN_POINT ( 'NONE',  ( 5.999999999999998224, 0.000000000000000000, 0.000000000000000000 ) ) ;
#4439=CARTESIAN_POINT ( 'NONE',  ( 0.000000000000000000, -1.249999999999999112, -6.997769477110050929 ) ) ;
#4487=AXIS2_PLACEMENT_3D ( 'NONE', #10000, #14179, #18897 ) ;
#4626=CARTESIAN_POINT ( 'NONE',  ( 0.000000000000000000, 0.000000000000000000, 0.000000000000000000 ) ) ;
#4764=CARTESIAN_POINT ( 'NONE',  ( 2.399999999999999911, -1.250000000000000444, 7.582700855991164168 ) ) ;
#4918=B_SPLINE_CURVE_WITH_KNOTS ( 'NONE', 3,
 ( #25502, #10561, #5818, #10420, #10281, #8407, #21188 ),
 .UNSPECIFIED., .F., .F.,
 ( 4, 3, 4 ),
 ( 0.01306422253233231051, 0.01395283648363494430, 0.01510707358649056309 ),
 .UNSPECIFIED. ) ;
#5150=EDGE_CURVE ( 'NONE', #14154, #5759, #19511, .T. ) ;
#5153=( NAMED_UNIT ( * ) SI_UNIT ( $, .STERADIAN. ) SOLID_ANGLE_UNIT ( ) );
#5197=( NAMED_UNIT ( * ) PLANE_ANGLE_UNIT ( ) SI_UNIT ( $, .RADIAN. ) );
#5199=ADVANCED_FACE ( 'NONE', ( #16472 ), #16894, .T. ) ;
#5428=EDGE_CURVE ( 'NONE', #21920, #3254, #27018, .T. ) ;
#5468=DIRECTION ( 'NONE',  ( 0.9961946980917455452, 1.067350013832299517E-17, 0.08715574274765836016 ) ) ;
#5480=PLANE ( 'NONE',  #27324 ) ;
#5593=VECTOR ( 'NONE', #6539, 1000.000000000000000 ) ;
#5603=APPLICATION_CONTEXT ( 'automotive_design' ) ;
#5624=FACE_OUTER_BOUND ( 'NONE', #10300, .T. ) ;
#5672=CONICAL_SURFACE ( 'NONE', #3837, 7.475068018844455153, 0.08726646259971666819 ) ;
#5683=CARTESIAN_POINT ( 'NONE',  ( 2.399999999999999911, 9.411460630883494610E-16, 7.685040811306673270 ) ) ;
#5744=B_SPLINE_CURVE_WITH_KNOTS ( 'NONE', 3,
 ( #25641, #21474, #12874, #25782, #1379, #1789 ),
 .UNSPECIFIED., .F., .F.,
 ( 4, 2, 4 ),
 ( 0.002183620363445708690, 0.002481209646569489634, 0.002778798929693271011 ),
 .UNSPECIFIED. ) ;
#5759=VERTEX_POINT ( 'NONE', #4439 ) ;
#5799=DIRECTION ( 'NONE',  ( 0.000000000000000000, 0.000000000000000000, 1.000000000000000000 ) ) ;
#5818=CARTESIAN_POINT ( 'NONE',  ( 0.9552291512637761661, 1.249999999999999556, -7.454565938624108767 ) ) ;
#5866=ORIENTED_EDGE ( 'NONE', *, *, #17290, .T. ) ;
#5888=CARTESIAN_POINT ( 'NONE',  ( 2.399999999999999911, 0.000000000000000000, 0.000000000000000000 ) ) ;
#6081=ORIENTED_EDGE ( 'NONE', *, *, #12030, .F. ) ;
#6159=AXIS2_PLACEMENT_3D ( 'NONE', #16363, #15940, #11916 ) ;
#6244=CARTESIAN_POINT ( 'NONE',  ( 0.000000000000000000, -1.249999999999998890, -8.000000000000000000 ) ) ;
#6293=ORIENTED_EDGE ( 'NONE', *, *, #5428, .F. ) ;
#6358=EDGE_CURVE ( 'NONE', #24118, #13603, #15154, .T. ) ;
#6433=VERTEX_POINT ( 'NONE', #25227 ) ;
#6539=DIRECTION ( 'NONE',  ( -1.000000000000000000, -0.000000000000000000, -0.000000000000000000 ) ) ;
#6665=AXIS2_PLACEMENT_3D ( 'NONE', #18059, #16055, #20348 ) ;
#6788=CARTESIAN_POINT ( 'NONE',  ( 2.399999999999999911, 1.249999999999999556, -8.000000000000000000 ) ) ;
#6855=AXIS2_PLACEMENT_3D ( 'NONE', #9796, #14111, #7361 ) ;
#6877=CARTESIAN_POINT ( 'NONE',  ( 40.99999999999999289, 0.000000000000000000, 5.000000000000000000 ) ) ;
#6948=DIRECTION ( 'NONE',  ( 1.000000000000000000, -0.000000000000000000, -0.000000000000000000 ) ) ;
#6987=CARTESIAN_POINT ( 'NONE',  ( 2.399999999999999911, -1.249999999999999112, -7.582700855991164168 ) ) ;
#7053=CARTESIAN_POINT ( 'NONE',  ( 5.999999999999998224, 9.797174393178825657E-16, 8.000000000000000000 ) ) ;
#7074=ORIENTED_EDGE ( 'NONE', *, *, #26401, .F. ) ;
#7150=ORIENTED_EDGE ( 'NONE', *, *, #7918, .T. ) ;
#7361=DIRECTION ( 'NONE',  ( 0.000000000000000000, 0.000000000000000000, 1.000000000000000000 ) ) ;
#7499=LINE ( 'NONE', #25148, #15802 ) ;
#7707=CARTESIAN_POINT ( 'NONE',  ( 0.1700960744404878267, -1.249999999999999112, -7.344776659773097016 ) ) ;
#7719=DIRECTION ( 'NONE',  ( 0.000000000000000000, -1.000000000000000000, -9.486769009248162565E-17 ) ) ;
#7784=CARTESIAN_POINT ( 'NONE',  ( 1.250275373174978055, 1.249999999999999556, 7.480737022738205511 ) ) ;
#7837=LINE ( 'NONE', #6244, #20479 ) ;
#7918=EDGE_CURVE ( 'NONE', #10893, #13603, #1865, .T. ) ;
#8052=DIRECTION ( 'NONE',  ( 1.000000000000000000, 0.000000000000000000, 0.000000000000000000 ) ) ;
#8123=CARTESIAN_POINT ( 'NONE',  ( 0.03761738457578049644, -1.249999999999998668, -7.196727321902812946 ) ) ;
#8132=LINE ( 'NONE', #25646, #5593 ) ;
#8238=CIRCLE ( 'NONE', #15584, 7.507013428474183847 ) ;
#8255=AXIS2_PLACEMENT_3D ( 'NONE', #23344, #18748, #21324 ) ;
#8299=CIRCLE ( 'NONE', #16122, 7.685040811306672381 ) ;
#8387=EDGE_CURVE ( 'NONE', #3645, #24118, #21046, .T. ) ;
#8395=ORIENTED_EDGE ( 'NONE', *, *, #6358, .F. ) ;
#8407=CARTESIAN_POINT ( 'NONE',  ( 2.016757918737201560, 1.249999999999999556, -7.548718989644206623 ) ) ;
#8422=ADVANCED_FACE ( 'NONE', ( #26669 ), #2251, .T. ) ;
#8427=CYLINDRICAL_SURFACE ( 'NONE', #14496, 5.000000000000000000 ) ;
#8671=DIRECTION ( 'NONE',  ( -1.000000000000000000, 0.000000000000000000, 0.000000000000000000 ) ) ;
#8743=EDGE_CURVE ( 'NONE', #19998, #24464, #8132, .T. ) ;
#9051=VECTOR ( 'NONE', #20005, 1000.000000000000000 ) ;
#9080=LINE ( 'NONE', #24172, #874 ) ;
#9135=ORIENTED_EDGE ( 'NONE', *, *, #8387, .T. ) ;
#9160=CARTESIAN_POINT ( 'NONE',  ( -6.124983682450844166E-17, 0.000000000000000000, 0.000000000000000000 ) ) ;
#9307=CIRCLE ( 'NONE', #15728, 7.108535549237485540 ) ;
#9426=VERTEX_POINT ( 'NONE', #22376 ) ;
#9725=CIRCLE ( 'NONE', #24392, 7.507013428474183847 ) ;
#9781=CYLINDRICAL_SURFACE ( 'NONE', #24761, 5.000000000000000000 ) ;
#9796=CARTESIAN_POINT ( 'NONE',  ( 5.999999999999998224, 0.000000000000000000, 0.000000000000000000 ) ) ;
#9913=ORIENTED_EDGE ( 'NONE', *, *, #1452, .F. ) ;
#9942=DIRECTION ( 'NONE',  ( 0.000000000000000000, 0.000000000000000000, 1.000000000000000000 ) ) ;
#9972=CARTESIAN_POINT ( 'NONE',  ( 0.3651377029009472697, 0.000000000000000000, 0.000000000000000000 ) ) ;
#10000=CARTESIAN_POINT ( 'NONE',  ( 0.000000000000000000, 0.000000000000000000, 0.000000000000000000 ) ) ;
#10035=( LENGTH_UNIT ( ) NAMED_UNIT ( * ) SI_UNIT ( .MILLI., .METRE. ) );
#10119=EDGE_LOOP ( 'NONE', ( #6081, #15248 ) ) ;
#10132=CARTESIAN_POINT ( 'NONE',  ( 2.399999999999999911, 0.000000000000000000, -7.685040811306673270 ) ) ;
#10217=PRODUCT_CONTEXT ( 'NONE', #5603, 'mechanical' ) ;
#10281=CARTESIAN_POINT ( 'NONE',  ( 1.633516369018861658, 1.249999999999999556, -7.514731128045610831 ) ) ;
#10300=EDGE_LOOP ( 'NONE', ( #12225, #22302 ) ) ;
#10362=DIRECTION ( 'NONE',  ( -1.000000000000000000, -0.000000000000000000, -0.000000000000000000 ) ) ;
#10420=CARTESIAN_POINT ( 'NONE',  ( 1.250275373174975835, 1.249999999999999556, -7.480737022738206399 ) ) ;
#10561=CARTESIAN_POINT ( 'NONE',  ( 0.6601832576049860846, 1.249999999999999556, -7.428391153593999263 ) ) ;
#10637=AXIS2_PLACEMENT_3D ( 'NONE', #25065, #2320, #14860 ) ;
#10882=CARTESIAN_POINT ( 'NONE',  ( 0.3651377028998192276, -1.249999999999998890, -7.402212548648222423 ) ) ;
#10893=VERTEX_POINT ( 'NONE', #5683 ) ;
#10942=ORIENTED_EDGE ( 'NONE', *, *, #16608, .F. ) ;
#10986=AXIS2_PLACEMENT_3D ( 'NONE', #4232, #26205, #13022 ) ;
#10991=CARTESIAN_POINT ( 'NONE',  ( 40.99999999999999289, 0.000000000000000000, 0.000000000000000000 ) ) ;
#11153=VECTOR ( 'NONE', #2853, 1000.000000000000000 ) ;
#11173=CARTESIAN_POINT ( 'NONE',  ( -5.421010862427522170E-17, -1.250000000000000444, 6.997769477110050929 ) ) ;
#11192=PRODUCT_DEFINITION_CONTEXT ( 'detailed design', #13339, 'design' ) ;
#11197=ADVANCED_FACE ( 'NONE', ( #2711 ), #1506, .T. ) ;
#11224=EDGE_LOOP ( 'NONE', ( #19963, #14085, #25203, #10942 ) ) ;
#11236=EDGE_CURVE ( 'NONE', #9426, #3254, #16235, .T. ) ;
#11424=CARTESIAN_POINT ( 'NONE',  ( 2.399999999999999911, 0.000000000000000000, 0.000000000000000000 ) ) ;
#11456=LINE ( 'NONE', #16330, #14 ) ;
#11499=DIRECTION ( 'NONE',  ( 0.000000000000000000, 0.000000000000000000, 1.000000000000000000 ) ) ;
#11704=FACE_OUTER_BOUND ( 'NONE', #12856, .T. ) ;
#11757=CARTESIAN_POINT ( 'NONE',  ( 0.3651377029009472142, -1.250000000000000444, 7.402212548643258394 ) ) ;
#11880=DIRECTION ( 'NONE',  ( -1.000000000000000000, -0.000000000000000000, -0.000000000000000000 ) ) ;
#11916=DIRECTION ( 'NONE',  ( 0.000000000000000000, 0.000000000000000000, 1.000000000000000000 ) ) ;
#11961=ORIENTED_EDGE ( 'NONE', *, *, #24650, .T. ) ;
#11970=ORIENTED_EDGE ( 'NONE', *, *, #7918, .F. ) ;
#12030=EDGE_CURVE ( 'NONE', #2218, #19998, #27679, .T. ) ;
#12125=DIRECTION ( 'NONE',  ( 0.000000000000000000, 1.000000000000000000, 0.000000000000000000 ) ) ;
#12179=B_SPLINE_CURVE_WITH_KNOTS ( 'NONE', 3,
 ( #6987, #26373, #24517, #388, #22075, #28374, #10882 ),
 .UNSPECIFIED., .F., .F.,
 ( 4, 3, 4 ),
 ( 0.01279859917594709795, 0.01395283628746606976, 0.01484145024773120096 ),
 .UNSPECIFIED. ) ;
#12225=ORIENTED_EDGE ( 'NONE', *, *, #15008, .F. ) ;
#12383=CARTESIAN_POINT ( 'NONE',  ( 41.00000000000000000, 5.000000000000000000, 0.000000000000000000 ) ) ;
#12450=CARTESIAN_POINT ( 'NONE',  ( 0.000000000000000000, -1.249999999999999112, -6.997769477110050929 ) ) ;
#12454=DIRECTION ( 'NONE',  ( 1.000000000000000000, -0.000000000000000000, -0.000000000000000000 ) ) ;
#12641=EDGE_LOOP ( 'NONE', ( #154, #21722 ) ) ;
#12647=ORIENTED_EDGE ( 'NONE', *, *, #18001, .F. ) ;
#12702=DIRECTION ( 'NONE',  ( -0.000000000000000000, 0.000000000000000000, 1.000000000000000000 ) ) ;
#12735=EDGE_CURVE ( 'NONE', #10893, #553, #7499, .T. ) ;
#12831=EDGE_LOOP ( 'NONE', ( #3627, #21200 ) ) ;
#12856=EDGE_LOOP ( 'NONE', ( #18602, #22526, #3601, #1193, #26204, #20323 ) ) ;
#12874=CARTESIAN_POINT ( 'NONE',  ( 0.03735363077137947296, 1.249999999999999556, -7.196572270765070556 ) ) ;
#12927=AXIS2_PLACEMENT_3D ( 'NONE', #9160, #19648, #17769 ) ;
#13022=DIRECTION ( 'NONE',  ( 0.000000000000000000, 0.000000000000000000, 1.000000000000000000 ) ) ;
#13032=CARTESIAN_POINT ( 'NONE',  ( -25.39999999999996305, 0.000000000000000000, 0.000000000000000000 ) ) ;
#13041=CARTESIAN_POINT ( 'NONE',  ( 0.3651377029009472697, 0.000000000000000000, 0.000000000000000000 ) ) ;
#13088=DIRECTION ( 'NONE',  ( 1.000000000000000000, -0.000000000000000000, -0.000000000000000000 ) ) ;
#13142=FACE_OUTER_BOUND ( 'NONE', #19737, .T. ) ;
#13149=CARTESIAN_POINT ( 'NONE',  ( 0.3651377028998192276, -1.249999999999998890, -7.402212548648222423 ) ) ;
#13211=UNCERTAINTY_MEASURE_WITH_UNIT (LENGTH_MEASURE( 1.000000000000000082E-05 ), #10035, 'distance_accuracy_value', 'NONE');
#13339=APPLICATION_CONTEXT ( 'automotive_design' ) ;
#13392=EDGE_LOOP ( 'NONE', ( #1901, #14160, #11961, #7074, #1632, #28001, #1984, #14091 ) ) ;
#13414=DIRECTION ( 'NONE',  ( 0.000000000000000000, 0.000000000000000000, -1.000000000000000000 ) ) ;
#13603=VERTEX_POINT ( 'NONE', #4764 ) ;
#13786=CARTESIAN_POINT ( 'NONE',  ( -5.421010862427522170E-17, 0.000000000000000000, 0.000000000000000000 ) ) ;
#13797=DIRECTION ( 'NONE',  ( 0.000000000000000000, 8.881784197001253901E-15, 1.000000000000000000 ) ) ;
#13941=CARTESIAN_POINT ( 'NONE',  ( 5.999999999999998224, 0.000000000000000000, -8.000000000000000000 ) ) ;
#14053=CARTESIAN_POINT ( 'NONE',  ( 0.6601832576049850854, -1.250000000000000444, 7.428391153593997487 ) ) ;
#14085=ORIENTED_EDGE ( 'NONE', *, *, #8743, .T. ) ;
#14091=ORIENTED_EDGE ( 'NONE', *, *, #25333, .F. ) ;
#14111=DIRECTION ( 'NONE',  ( -1.000000000000000000, -0.000000000000000000, -0.000000000000000000 ) ) ;
#14145=SHAPE_REPRESENTATION ( 'slotted cheese head screw_iso_ISO 1207 - M10 x 35 - 35N', ( #10637 ), #25313 ) ;
#14154=VERTEX_POINT ( 'NONE', #13149 ) ;
#14160=ORIENTED_EDGE ( 'NONE', *, *, #12735, .T. ) ;
#14176=AXIS2_PLACEMENT_3D ( 'NONE', #3664, #12454, #14461 ) ;
#14179=DIRECTION ( 'NONE',  ( 1.000000000000000000, 0.000000000000000000, 0.000000000000000000 ) ) ;
#14275=DIRECTION ( 'NONE',  ( 0.000000000000000000, -0.000000000000000000, 1.000000000000000000 ) ) ;
#14308=CARTESIAN_POINT ( 'NONE',  ( 2.399999999999999911, -1.249999999999999112, -7.582700855991164168 ) ) ;
#14329=ORIENTED_EDGE ( 'NONE', *, *, #14639, .F. ) ;
#14400=CARTESIAN_POINT ( 'NONE',  ( 0.9552291512637774984, 1.249999999999999556, 7.454565938624106991 ) ) ;
#14461=DIRECTION ( 'NONE',  ( 0.000000000000000000, -1.598721155460225418E-14, 1.000000000000000000 ) ) ;
#14496=AXIS2_PLACEMENT_3D ( 'NONE', #13032, #28355, #17182 ) ;
#14504=ORIENTED_EDGE ( 'NONE', *, *, #27376, .F. ) ;
#14507=VERTEX_POINT ( 'NONE', #13941 ) ;
#14639=EDGE_CURVE ( 'NONE', #1600, #14154, #12179, .T. ) ;
#14640=AXIS2_PLACEMENT_3D ( 'NONE', #21158, #3626, #12702 ) ;
#14645=AXIS2_PLACEMENT_3D ( 'NONE', #11424, #6948, #16020 ) ;
#14687=ORIENTED_EDGE ( 'NONE', *, *, #16207, .T. ) ;
#14743=( GEOMETRIC_REPRESENTATION_CONTEXT ( 3 ) GLOBAL_UNCERTAINTY_ASSIGNED_CONTEXT ( ( #13211 ) ) GLOBAL_UNIT_ASSIGNED_CONTEXT ( ( #10035, #22965, #5153 ) ) REPRESENTATION_CONTEXT ( 'NONE', 'WORKASPACE' ) );
#14781=ORIENTED_EDGE ( 'NONE', *, *, #25482, .T. ) ;
#14860=DIRECTION ( 'NONE',  ( 1.000000000000000000, 0.000000000000000000, 0.000000000000000000 ) ) ;
#14980=CIRCLE ( 'NONE', #23225, 5.000000000000000000 ) ;
#14999=EDGE_CURVE ( 'NONE', #1788, #3254, #4918, .T. ) ;
#15008=EDGE_CURVE ( 'NONE', #5759, #3645, #7837, .T. ) ;
#15091=DIRECTION ( 'NONE',  ( 0.000000000000000000, 0.000000000000000000, 1.000000000000000000 ) ) ;
#15154=B_SPLINE_CURVE_WITH_KNOTS ( 'NONE', 3,
 ( #11757, #14053, #22802, #20497, #25643, #16890, #3812 ),
 .UNSPECIFIED., .F., .F.,
 ( 4, 3, 4 ),
 ( 0.01306422253233230878, 0.01395283648363494430, 0.01510707358649056309 ),
 .UNSPECIFIED. ) ;
#15156=CARTESIAN_POINT ( 'NONE',  ( 0.1707425712781837635, 1.249999999999999556, 7.345313475977262030 ) ) ;
#15158=B_SPLINE_CURVE_WITH_KNOTS ( 'NONE', 3,
 ( #15565, #16692, #25443, #7784, #14400, #23153, #16415 ),
 .UNSPECIFIED., .F., .F.,
 ( 4, 3, 4 ),
 ( 0.01279859917594709795, 0.01395283628746607149, 0.01484145024773051748 ),
 .UNSPECIFIED. ) ;
#15176=EDGE_LOOP ( 'NONE', ( #17732, #20157, #3171, #12647 ) ) ;
#15248=ORIENTED_EDGE ( 'NONE', *, *, #25482, .F. ) ;
#15385=CARTESIAN_POINT ( 'NONE',  ( 40.99999999999999289, 6.123233995736766282E-16, -5.000000000000000000 ) ) ;
#15565=CARTESIAN_POINT ( 'NONE',  ( 2.399999999999999911, 1.249999999999999556, 7.582700855991164168 ) ) ;
#15569=DIRECTION ( 'NONE',  ( 0.000000000000000000, 0.000000000000000000, 1.000000000000000000 ) ) ;
#15582=AXIS2_PLACEMENT_3D ( 'NONE', #12383, #8052, #18688 ) ;
#15584=AXIS2_PLACEMENT_3D ( 'NONE', #13041, #21788, #21639 ) ;
#15706=SHAPE_REPRESENTATION_RELATIONSHIP ( 'NONE' , 'NONE' ,  #14145, #24247 ) ;
#15727=CARTESIAN_POINT ( 'NONE',  ( -5.421010862427522170E-17, -1.250000000000000444, 6.997769477110050929 ) ) ;
#15728=AXIS2_PLACEMENT_3D ( 'NONE', #13786, #16081, #26009 ) ;
#15802=VECTOR ( 'NONE', #5468, 1000.000000000000000 ) ;
#15810=DIRECTION ( 'NONE',  ( 1.000000000000000000, -0.000000000000000000, -0.000000000000000000 ) ) ;
#15940=DIRECTION ( 'NONE',  ( -1.000000000000000000, -0.000000000000000000, -0.000000000000000000 ) ) ;
#16020=DIRECTION ( 'NONE',  ( 0.000000000000000000, 0.000000000000000000, 1.000000000000000000 ) ) ;
#16055=DIRECTION ( 'NONE',  ( -1.000000000000000000, -0.000000000000000000, -0.000000000000000000 ) ) ;
#16079=EDGE_CURVE ( 'NONE', #9426, #10893, #1317, .T. ) ;
#16081=DIRECTION ( 'NONE',  ( -1.000000000000000000, -0.000000000000000000, -0.000000000000000000 ) ) ;
#16092=EDGE_CURVE ( 'NONE', #3858, #1788, #5744, .T. ) ;
#16122=AXIS2_PLACEMENT_3D ( 'NONE', #24024, #15810, #13797 ) ;
#16133=ORIENTED_EDGE ( 'NONE', *, *, #17290, .F. ) ;
#16207=EDGE_CURVE ( 'NONE', #14507, #553, #27473, .T. ) ;
#16235=LINE ( 'NONE', #26697, #11153 ) ;
#16330=CARTESIAN_POINT ( 'NONE',  ( 2.399999999999999911, -1.249999999999998890, -8.000000000000000000 ) ) ;
#16363=CARTESIAN_POINT ( 'NONE',  ( -5.421010862427522170E-17, 0.000000000000000000, 0.000000000000000000 ) ) ;
#16391=CARTESIAN_POINT ( 'NONE',  ( 0.3651377029009472142, 1.249999999999999556, 7.402212548643259282 ) ) ;
#16415=CARTESIAN_POINT ( 'NONE',  ( 0.3651377029009472142, 1.249999999999999556, 7.402212548643259282 ) ) ;
#16472=FACE_OUTER_BOUND ( 'NONE', #13392, .T. ) ;
#16485=DIRECTION ( 'NONE',  ( 0.000000000000000000, 9.486769009248162565E-17, -1.000000000000000000 ) ) ;
#16497=ADVANCED_FACE ( 'NONE', ( #25891, #23457 ), #18863, .F. ) ;
#16608=EDGE_CURVE ( 'NONE', #2218, #6433, #9080, .T. ) ;
#16692=CARTESIAN_POINT ( 'NONE',  ( 2.016757918737204225, 1.249999999999999556, 7.548718989644206623 ) ) ;
#16737=EDGE_CURVE ( 'NONE', #6433, #24464, #451, .T. ) ;
#16839=ADVANCED_FACE ( 'NONE', ( #27998 ), #23284, .T. ) ;
#16890=CARTESIAN_POINT ( 'NONE',  ( 2.016757918737201560, -1.250000000000000444, 7.548718989644205735 ) ) ;
#16894=CONICAL_SURFACE ( 'NONE', #4487, 7.475068018844455153, 0.08726646259971666819 ) ;
#17182=DIRECTION ( 'NONE',  ( 0.000000000000000000, 0.000000000000000000, 1.000000000000000000 ) ) ;
#17290=EDGE_CURVE ( 'NONE', #1600, #13603, #11456, .T. ) ;
#17335=CARTESIAN_POINT ( 'NONE',  ( 5.999999999999998224, 6.123233995736766282E-16, -5.000000000000000000 ) ) ;
#17360=ADVANCED_FACE ( 'NONE', ( #19031 ), #22941, .T. ) ;
#17633=CARTESIAN_POINT ( 'NONE',  ( 0.1707501505551958787, -1.250000000000000444, 7.345390377919865266 ) ) ;
#17732=ORIENTED_EDGE ( 'NONE', *, *, #16092, .F. ) ;
#17769=DIRECTION ( 'NONE',  ( -0.000000000000000000, 0.000000000000000000, 1.000000000000000000 ) ) ;
#17839=DIRECTION ( 'NONE',  ( -1.000000000000000000, -0.000000000000000000, -0.000000000000000000 ) ) ;
#18001=EDGE_CURVE ( 'NONE', #1788, #761, #9725, .T. ) ;
#18059=CARTESIAN_POINT ( 'NONE',  ( 5.999999999999998224, 0.000000000000000000, 0.000000000000000000 ) ) ;
#18069=CARTESIAN_POINT ( 'NONE',  ( 0.3651377029009472142, -1.250000000000000444, 7.402212548643258394 ) ) ;
#18097=DIRECTION ( 'NONE',  ( -1.000000000000000000, -0.000000000000000000, -0.000000000000000000 ) ) ;
#18140=AXIS2_PLACEMENT_3D ( 'NONE', #2665, #11880, #669 ) ;
#18261=FACE_OUTER_BOUND ( 'NONE', #20185, .T. ) ;
#18406=EDGE_CURVE ( 'NONE', #1600, #21920, #8299, .T. ) ;
#18502=MANIFOLD_SOLID_BREP ( 'Slot', #21427 ) ;
#18602=ORIENTED_EDGE ( 'NONE', *, *, #14999, .T. ) ;
#18608=CIRCLE ( 'NONE', #6665, 8.000000000000000000 ) ;
#18633=PLANE ( 'NONE',  #27776 ) ;
#18688=DIRECTION ( 'NONE',  ( 0.000000000000000000, 0.000000000000000000, -1.000000000000000000 ) ) ;
#18748=DIRECTION ( 'NONE',  ( -1.000000000000000000, -0.000000000000000000, -0.000000000000000000 ) ) ;
#18863=PLANE ( 'NONE',  #14640 ) ;
#18897=DIRECTION ( 'NONE',  ( 0.000000000000000000, 0.000000000000000000, -1.000000000000000000 ) ) ;
#19031=FACE_OUTER_BOUND ( 'NONE', #15176, .T. ) ;
#19036=DIRECTION ( 'NONE',  ( 0.000000000000000000, -9.486769009248163798E-17, 1.000000000000000000 ) ) ;
#19167=CARTESIAN_POINT ( 'NONE',  ( 0.2663009637210750902, 1.249999999999999556, 7.393443028451041954 ) ) ;
#19509=ORIENTED_EDGE ( 'NONE', *, *, #21537, .T. ) ;
#19511=B_SPLINE_CURVE_WITH_KNOTS ( 'NONE', 3,
 ( #27506, #21048, #7707, #8123, #3380, #12450 ),
 .UNSPECIFIED., .F., .F.,
 ( 4, 2, 4 ),
 ( 0.002263534818064183874, 0.002560835764897306972, 0.002858136711730429637 ),
 .UNSPECIFIED. ) ;
#19601=EDGE_LOOP ( 'NONE', ( #5866, #11970, #379, #23970, #6293, #25169 ) ) ;
#19648=DIRECTION ( 'NONE',  ( -1.000000000000000000, 0.000000000000000000, -0.000000000000000000 ) ) ;
#19737=EDGE_LOOP ( 'NONE', ( #22162, #7150, #8395, #3112, #14329, #22208, #26662, #14687 ) ) ;
#19864=PLANE ( 'NONE',  #3050 ) ;
#19963=ORIENTED_EDGE ( 'NONE', *, *, #12030, .T. ) ;
#19998=VERTEX_POINT ( 'NONE', #15385 ) ;
#20005=DIRECTION ( 'NONE',  ( 0.9961946980917455452, 0.000000000000000000, -0.08715574274765836016 ) ) ;
#20066=CARTESIAN_POINT ( 'NONE',  ( 0.03738397811494300477, -1.250000000000000666, 7.196583346711943108 ) ) ;
#20157=ORIENTED_EDGE ( 'NONE', *, *, #21537, .F. ) ;
#20185=EDGE_LOOP ( 'NONE', ( #2435, #14781, #24966, #9913 ) ) ;
#20323=ORIENTED_EDGE ( 'NONE', *, *, #16092, .T. ) ;
#20348=DIRECTION ( 'NONE',  ( 0.000000000000000000, 0.000000000000000000, 1.000000000000000000 ) ) ;
#20426=( NAMED_UNIT ( * ) SI_UNIT ( $, .STERADIAN. ) SOLID_ANGLE_UNIT ( ) );
#20437=LINE ( 'NONE', #26760, #9051 ) ;
#20479=VECTOR ( 'NONE', #19036, 1000.000000000000000 ) ;
#20497=CARTESIAN_POINT ( 'NONE',  ( 1.250275373174976279, -1.250000000000000444, 7.480737022738205511 ) ) ;
#21046=B_SPLINE_CURVE_WITH_KNOTS ( 'NONE', 3,
 ( #11173, #21943, #20066, #17633, #21807, #18069 ),
 .UNSPECIFIED., .F., .F.,
 ( 4, 2, 4 ),
 ( 0.0003697107221120765510, 0.0006673033929023622877, 0.0009648960636926479702 ),
 .UNSPECIFIED. ) ;
#21048=CARTESIAN_POINT ( 'NONE',  ( 0.2662533044063318810, -1.249999999999998890, -7.393438799766935965 ) ) ;
#21065=FACE_OUTER_BOUND ( 'NONE', #25766, .T. ) ;
#21125=ORIENTED_EDGE ( 'NONE', *, *, #23134, .F. ) ;
#21158=CARTESIAN_POINT ( 'NONE',  ( 5.999999999999999112, 5.000000000000000000, 0.000000000000000000 ) ) ;
#21188=CARTESIAN_POINT ( 'NONE',  ( 2.399999999999999911, 1.249999999999999556, -7.582700855991164168 ) ) ;
#21200=ORIENTED_EDGE ( 'NONE', *, *, #1452, .T. ) ;
#21253=ADVANCED_FACE ( 'NONE', ( #13142 ), #5672, .T. ) ;
#21284=CIRCLE ( 'NONE', #6159, 7.108535549237485540 ) ;
#21324=DIRECTION ( 'NONE',  ( 0.000000000000000000, 0.000000000000000000, 1.000000000000000000 ) ) ;
#21427=CLOSED_SHELL ( 'NONE', ( #5199, #24984, #8422, #17360, #779, #16839, #25354, #21253, #16497, #11197, #23490, #24888, #26279 ) ) ;
#21474=CARTESIAN_POINT ( 'NONE',  ( -3.853576393533437815E-15, 1.249999999999999556, -7.097445415343742958 ) ) ;
#21537=EDGE_CURVE ( 'NONE', #26048, #3858, #9307, .T. ) ;
#21639=DIRECTION ( 'NONE',  ( 0.000000000000000000, 0.000000000000000000, 1.000000000000000000 ) ) ;
#21722=ORIENTED_EDGE ( 'NONE', *, *, #24650, .F. ) ;
#21788=DIRECTION ( 'NONE',  ( 1.000000000000000000, 0.000000000000000000, 0.000000000000000000 ) ) ;
#21807=CARTESIAN_POINT ( 'NONE',  ( 0.2651721261003159302, -1.250000000000000444, 7.393342869700422426 ) ) ;
#21852=ORIENTED_EDGE ( 'NONE', *, *, #8387, .F. ) ;
#21883=DIRECTION ( 'NONE',  ( 1.000000000000000000, 0.000000000000000000, 0.000000000000000000 ) ) ;
#21920=VERTEX_POINT ( 'NONE', #10132 ) ;
#21943=CARTESIAN_POINT ( 'NONE',  ( -8.294146619514105765E-15, -1.250000000000000222, 7.097209492490607730 ) ) ;
#22075=CARTESIAN_POINT ( 'NONE',  ( 0.9552291512635501247, -1.249999999999998890, -7.454565938624087451 ) ) ;
#22162=ORIENTED_EDGE ( 'NONE', *, *, #12735, .F. ) ;
#22208=ORIENTED_EDGE ( 'NONE', *, *, #18406, .T. ) ;
#22302=ORIENTED_EDGE ( 'NONE', *, *, #23134, .T. ) ;
#22376=CARTESIAN_POINT ( 'NONE',  ( 2.399999999999999911, 1.249999999999999556, 7.582700855991164168 ) ) ;
#22526=ORIENTED_EDGE ( 'NONE', *, *, #11236, .F. ) ;
#22667=AXIS2_PLACEMENT_3D ( 'NONE', #10991, #26625, #24335 ) ;
#22713=CARTESIAN_POINT ( 'NONE',  ( -25.39999999999996305, 0.000000000000000000, 0.000000000000000000 ) ) ;
#22802=CARTESIAN_POINT ( 'NONE',  ( 0.9552291512637759441, -1.250000000000000444, 7.454565938624107879 ) ) ;
#22821=CARTESIAN_POINT ( 'NONE',  ( 0.000000000000000000, 1.249999999999999556, 8.000000000000000000 ) ) ;
#22885=CARTESIAN_POINT ( 'NONE',  ( 2.399999999999999911, 1.249999999999999556, 8.000000000000000000 ) ) ;
#22941=TOROIDAL_SURFACE ( 'NONE', #8255, 7.108535549237485540, 0.4000000000000000222 ) ;
#22965=( NAMED_UNIT ( * ) PLANE_ANGLE_UNIT ( ) SI_UNIT ( $, .RADIAN. ) );
#23067=EDGE_CURVE ( 'NONE', #26048, #3858, #26842, .T. ) ;
#23134=EDGE_CURVE ( 'NONE', #5759, #3645, #21284, .T. ) ;
#23153=CARTESIAN_POINT ( 'NONE',  ( 0.6601832576049863066, 1.249999999999999556, 7.428391153593998375 ) ) ;
#23218=EDGE_CURVE ( 'NONE', #761, #26048, #3532, .T. ) ;
#23225=AXIS2_PLACEMENT_3D ( 'NONE', #1172, #10362, #9942 ) ;
#23284=PLANE ( 'NONE',  #15582 ) ;
#23344=CARTESIAN_POINT ( 'NONE',  ( 0.3999999999999999667, 0.000000000000000000, 0.000000000000000000 ) ) ;
#23457=FACE_BOUND ( 'NONE', #12831, .T. ) ;
#23482=CARTESIAN_POINT ( 'NONE',  ( 0.03763830711997131345, 1.249999999999999556, 7.196935439755601571 ) ) ;
#23490=ADVANCED_FACE ( 'NONE', ( #11704 ), #27320, .F. ) ;
#23600=EDGE_LOOP ( 'NONE', ( #27626, #19509 ) ) ;
#23609=AXIS2_PLACEMENT_3D ( 'NONE', #22885, #12125, #14275 ) ;
#23909=CARTESIAN_POINT ( 'NONE',  ( -5.421010862427522170E-17, 1.249999999999999778, 7.098227728112298962 ) ) ;
#23970=ORIENTED_EDGE ( 'NONE', *, *, #11236, .T. ) ;
#24024=CARTESIAN_POINT ( 'NONE',  ( 2.399999999999999911, 0.000000000000000000, 0.000000000000000000 ) ) ;
#24049=ORIENTED_EDGE ( 'NONE', *, *, #5150, .T. ) ;
#24118=VERTEX_POINT ( 'NONE', #27705 ) ;
#24172=CARTESIAN_POINT ( 'NONE',  ( -25.39999999999996305, 0.000000000000000000, 5.000000000000000000 ) ) ;
#24184=FACE_OUTER_BOUND ( 'NONE', #19601, .T. ) ;
#24247=ADVANCED_BREP_SHAPE_REPRESENTATION ( '', ( #18502, #10637 ), #25313 ) ;
#24253=ORIENTED_EDGE ( 'NONE', *, *, #14639, .T. ) ;
#24335=DIRECTION ( 'NONE',  ( 0.000000000000000000, 0.000000000000000000, 1.000000000000000000 ) ) ;
#24392=AXIS2_PLACEMENT_3D ( 'NONE', #9972, #1625, #5799 ) ;
#24464=VERTEX_POINT ( 'NONE', #17335 ) ;
#24517=CARTESIAN_POINT ( 'NONE',  ( 1.633516369018864323, -1.249999999999998890, -7.514731128045609942 ) ) ;
#24650=EDGE_CURVE ( 'NONE', #553, #14507, #18608, .T. ) ;
#24721=CARTESIAN_POINT ( 'NONE',  ( 2.399999999999999911, 1.249999999999999556, -7.582700855991164168 ) ) ;
#24761=AXIS2_PLACEMENT_3D ( 'NONE', #22713, #25004, #27150 ) ;
#24888=ADVANCED_FACE ( 'NONE', ( #21065 ), #18633, .F. ) ;
#24941=DIRECTION ( 'NONE',  ( 0.000000000000000000, -9.486769009248163798E-17, 1.000000000000000000 ) ) ;
#24966=ORIENTED_EDGE ( 'NONE', *, *, #16608, .T. ) ;
#24984=ADVANCED_FACE ( 'NONE', ( #2220 ), #8427, .T. ) ;
#25004=DIRECTION ( 'NONE',  ( -1.000000000000000000, -0.000000000000000000, -0.000000000000000000 ) ) ;
#25065=CARTESIAN_POINT ( 'NONE',  ( 0.000000000000000000, 0.000000000000000000, 0.000000000000000000 ) ) ;
#25107=DIRECTION ( 'NONE',  ( 0.000000000000000000, 0.000000000000000000, -1.000000000000000000 ) ) ;
#25148=CARTESIAN_POINT ( 'NONE',  ( 0.000000000000000000, 9.154318122686608561E-16, 7.475068018844455153 ) ) ;
#25169=ORIENTED_EDGE ( 'NONE', *, *, #18406, .F. ) ;
#25203=ORIENTED_EDGE ( 'NONE', *, *, #16737, .F. ) ;
#25227=CARTESIAN_POINT ( 'NONE',  ( 5.999999999999998224, 0.000000000000000000, 5.000000000000000000 ) ) ;
#25313=( GEOMETRIC_REPRESENTATION_CONTEXT ( 3 ) GLOBAL_UNCERTAINTY_ASSIGNED_CONTEXT ( ( #840 ) ) GLOBAL_UNIT_ASSIGNED_CONTEXT ( ( #2464, #5197, #20426 ) ) REPRESENTATION_CONTEXT ( 'NONE', 'WORKASPACE' ) );
#25333=EDGE_CURVE ( 'NONE', #9426, #761, #15158, .T. ) ;
#25354=ADVANCED_FACE ( 'NONE', ( #5624 ), #5480, .T. ) ;
#25443=CARTESIAN_POINT ( 'NONE',  ( 1.633516369018864101, 1.249999999999999556, 7.514731128045609942 ) ) ;
#25482=EDGE_CURVE ( 'NONE', #19998, #2218, #14980, .T. ) ;
#25487=CARTESIAN_POINT ( 'NONE',  ( 0.000000000000000000, 1.249999999999999556, 6.997769477110050929 ) ) ;
#25502=CARTESIAN_POINT ( 'NONE',  ( 0.3651377029009472142, 1.249999999999999556, -7.402212548643259282 ) ) ;
#25569=SHAPE_DEFINITION_REPRESENTATION ( #4067, #14145 ) ;
#25635=PRODUCT_DEFINITION ( 'UNKNOWN', '', #25780, #11192 ) ;
#25641=CARTESIAN_POINT ( 'NONE',  ( 0.000000000000000000, 1.249999999999999556, -6.997769477110050929 ) ) ;
#25643=CARTESIAN_POINT ( 'NONE',  ( 1.633516369018862102, -1.250000000000000444, 7.514731128045609942 ) ) ;
#25646=CARTESIAN_POINT ( 'NONE',  ( -25.39999999999996305, 6.123233995736766282E-16, -5.000000000000000000 ) ) ;
#25736=AXIS2_PLACEMENT_3D ( 'NONE', #5888, #13088, #15091 ) ;
#25766=EDGE_LOOP ( 'NONE', ( #24253, #24049, #1201, #9135, #3245, #16133 ) ) ;
#25769=CARTESIAN_POINT ( 'NONE',  ( 0.3651377029009472142, 1.249999999999999556, 7.402212548643259282 ) ) ;
#25780=PRODUCT_DEFINITION_FORMATION_WITH_SPECIFIED_SOURCE ( 'ANY', '', #1547, .NOT_KNOWN. ) ;
#25782=CARTESIAN_POINT ( 'NONE',  ( 0.1708624500919104228, 1.249999999999999556, -7.345492880323159390 ) ) ;
#25891=FACE_OUTER_BOUND ( 'NONE', #12641, .T. ) ;
#26009=DIRECTION ( 'NONE',  ( 0.000000000000000000, 0.000000000000000000, 1.000000000000000000 ) ) ;
#26048=VERTEX_POINT ( 'NONE', #25487 ) ;
#26204=ORIENTED_EDGE ( 'NONE', *, *, #23067, .T. ) ;
#26205=DIRECTION ( 'NONE',  ( -1.000000000000000000, -0.000000000000000000, -0.000000000000000000 ) ) ;
#26279=ADVANCED_FACE ( 'NONE', ( #24184 ), #19864, .T. ) ;
#26373=CARTESIAN_POINT ( 'NONE',  ( 2.016757918737204225, -1.249999999999998890, -7.548718989644206623 ) ) ;
#26401=EDGE_CURVE ( 'NONE', #21920, #14507, #20437, .T. ) ;
#26625=DIRECTION ( 'NONE',  ( -1.000000000000000000, -0.000000000000000000, -0.000000000000000000 ) ) ;
#26662=ORIENTED_EDGE ( 'NONE', *, *, #26401, .T. ) ;
#26669=FACE_OUTER_BOUND ( 'NONE', #23600, .T. ) ;
#26697=CARTESIAN_POINT ( 'NONE',  ( 2.399999999999999911, 1.249999999999999556, 8.000000000000000000 ) ) ;
#26760=CARTESIAN_POINT ( 'NONE',  ( 0.000000000000000000, 0.000000000000000000, -7.475068018844455153 ) ) ;
#26842=LINE ( 'NONE', #22821, #2469 ) ;
#26963=ORIENTED_EDGE ( 'NONE', *, *, #5150, .F. ) ;
#27018=CIRCLE ( 'NONE', #14645, 7.685040811306672381 ) ;
#27051=CARTESIAN_POINT ( 'NONE',  ( 0.000000000000000000, 1.249999999999999556, -6.997769477110050929 ) ) ;
#27150=DIRECTION ( 'NONE',  ( 0.000000000000000000, 0.000000000000000000, 1.000000000000000000 ) ) ;
#27199=AXIS2_PLACEMENT_3D ( 'NONE', #427, #18097, #11499 ) ;
#27320=PLANE ( 'NONE',  #23609 ) ;
#27324=AXIS2_PLACEMENT_3D ( 'NONE', #3461, #1032, #1312 ) ;
#27376=EDGE_CURVE ( 'NONE', #24118, #14154, #8238, .T. ) ;
#27377=CARTESIAN_POINT ( 'NONE',  ( 2.399999999999999911, -1.249999999999998890, -8.000000000000000000 ) ) ;
#27473=CIRCLE ( 'NONE', #10986, 8.000000000000000000 ) ;
#27506=CARTESIAN_POINT ( 'NONE',  ( 0.3651377028998192276, -1.249999999999998890, -7.402212548648222423 ) ) ;
#27626=ORIENTED_EDGE ( 'NONE', *, *, #23067, .F. ) ;
#27679=CIRCLE ( 'NONE', #22667, 5.000000000000000000 ) ;
#27705=CARTESIAN_POINT ( 'NONE',  ( 0.3651377029009472142, -1.250000000000000444, 7.402212548643258394 ) ) ;
#27776=AXIS2_PLACEMENT_3D ( 'NONE', #27377, #7719, #16485 ) ;
#27998=FACE_OUTER_BOUND ( 'NONE', #10119, .T. ) ;
#28001=ORIENTED_EDGE ( 'NONE', *, *, #14999, .F. ) ;
#28224=EDGE_LOOP ( 'NONE', ( #26963, #14504, #21852, #21125 ) ) ;
#28355=DIRECTION ( 'NONE',  ( -1.000000000000000000, -0.000000000000000000, -0.000000000000000000 ) ) ;
#28374=CARTESIAN_POINT ( 'NONE',  ( 0.6601832576045314482, -1.249999999999998890, -7.428391153593958407 ) ) ;
#28442=COLOUR_RGB('Black',0.12,0.14,0.17);
#28443=FILL_AREA_STYLE_COLOUR('',#28442);
#28444=FILL_AREA_STYLE('',(#28443));
#28445=SURFACE_STYLE_FILL_AREA(#28444);
#28446=SURFACE_SIDE_STYLE('',(#28445));
#28447=SURFACE_STYLE_USAGE(.BOTH.,#28446);
#28448=PRESENTATION_STYLE_ASSIGNMENT((#28447));
ENDSEC;
END-ISO-10303-21;
